ISO-10303-21;
HEADER;
/* Generated by software containing ST-Developer
 * from STEP Tools, Inc. (www.steptools.com) 
 */

FILE_DESCRIPTION(
/* description */ (''),
/* implementation_level */ '2;1');

FILE_NAME(
/* name */ 'Cap Screw - M4x16.step',
/* time_stamp */ '2026-10-29T16:43:51-07:00',
/* author */ (''),
/* organization */ (''),
/* preprocessor_version */ 'ST-DEVELOPER v20.2',
/* originating_system */ 'Autodesk Translation Framework v15.17.0.0',
/* authorisation */ '');

FILE_SCHEMA (('AUTOMOTIVE_DESIGN { 1 0 10303 214 3 1 1 }'));
ENDSEC;

DATA;
#10=MECHANICAL_DESIGN_GEOMETRIC_PRESENTATION_REPRESENTATION('',(#383),#10292);
#285=ORIENTED_CLOSED_SHELL('',*,#5028,.F.);
#290=BREP_WITH_VOIDS('Body1',#5027,(#285));
#307=CONICAL_SURFACE('',#5711,0.325,0.785398163397448);
#308=CONICAL_SURFACE('',#5715,0.335,0.785398163397448);
#309=CONICAL_SURFACE('',#5719,0.21,0.463647609000806);
#310=CONICAL_SURFACE('',#5723,0.18,0.785398163397448);
#337=SHAPE_REPRESENTATION_RELATIONSHIP('SRR','None',#10435,#360);
#360=ADVANCED_BREP_SHAPE_REPRESENTATION('',(#290),#10287);
#383=STYLED_ITEM('',(#10635),#290);
#524=FACE_BOUND('',#1350,.T.);
#673=PLANE('',#5709);
#674=PLANE('',#5717);
#675=PLANE('',#5725);
#676=PLANE('',#5726);
#677=PLANE('',#5727);
#678=PLANE('',#5728);
#679=PLANE('',#5729);
#680=PLANE('',#5730);
#681=PLANE('',#5731);
#682=PLANE('',#5732);
#683=PLANE('',#5733);
#939=FACE_OUTER_BOUND('',#1345,.T.);
#940=FACE_OUTER_BOUND('',#1346,.T.);
#941=FACE_OUTER_BOUND('',#1347,.T.);
#942=FACE_OUTER_BOUND('',#1348,.T.);
#943=FACE_OUTER_BOUND('',#1349,.T.);
#944=FACE_OUTER_BOUND('',#1351,.T.);
#945=FACE_OUTER_BOUND('',#1352,.T.);
#946=FACE_OUTER_BOUND('',#1353,.T.);
#947=FACE_OUTER_BOUND('',#1354,.T.);
#948=FACE_OUTER_BOUND('',#1355,.T.);
#949=FACE_OUTER_BOUND('',#1356,.T.);
#950=FACE_OUTER_BOUND('',#1357,.T.);
#951=FACE_OUTER_BOUND('',#1358,.T.);
#952=FACE_OUTER_BOUND('',#1359,.T.);
#953=FACE_OUTER_BOUND('',#1360,.T.);
#954=FACE_OUTER_BOUND('',#1361,.T.);
#955=FACE_OUTER_BOUND('',#1362,.T.);
#1345=EDGE_LOOP('',(#4421));
#1346=EDGE_LOOP('',(#4422,#4423,#4424,#4425));
#1347=EDGE_LOOP('',(#4426,#4427,#4428,#4429));
#1348=EDGE_LOOP('',(#4430,#4431,#4432,#4433));
#1349=EDGE_LOOP('',(#4434));
#1350=EDGE_LOOP('',(#4435));
#1351=EDGE_LOOP('',(#4436,#4437,#4438,#4439));
#1352=EDGE_LOOP('',(#4440,#4441,#4442,#4443));
#1353=EDGE_LOOP('',(#4444,#4445,#4446,#4447));
#1354=EDGE_LOOP('',(#4448));
#1355=EDGE_LOOP('',(#4449,#4450,#4451,#4452));
#1356=EDGE_LOOP('',(#4453,#4454,#4455,#4456));
#1357=EDGE_LOOP('',(#4457,#4458,#4459,#4460));
#1358=EDGE_LOOP('',(#4461,#4462,#4463,#4464));
#1359=EDGE_LOOP('',(#4465,#4466,#4467,#4468));
#1360=EDGE_LOOP('',(#4469,#4470,#4471,#4472));
#1361=EDGE_LOOP('',(#4473,#4474,#4475,#4476,#4477,#4478));
#1362=EDGE_LOOP('',(#4479,#4480,#4481,#4482,#4483,#4484));
#1727=LINE('',#9944,#2119);
#1728=LINE('',#9948,#2120);
#1729=LINE('',#9952,#2121);
#1730=LINE('',#9959,#2122);
#1731=LINE('',#9963,#2123);
#1732=LINE('',#9967,#2124);
#1733=LINE('',#9972,#2125);
#1734=LINE('',#9974,#2126);
#1735=LINE('',#9976,#2127);
#1736=LINE('',#9977,#2128);
#1737=LINE('',#9980,#2129);
#1738=LINE('',#9982,#2130);
#1739=LINE('',#9983,#2131);
#1740=LINE('',#9986,#2132);
#1741=LINE('',#9988,#2133);
#1742=LINE('',#9989,#2134);
#1743=LINE('',#9992,#2135);
#1744=LINE('',#9994,#2136);
#1745=LINE('',#9995,#2137);
#1746=LINE('',#9998,#2138);
#1747=LINE('',#10000,#2139);
#1748=LINE('',#10001,#2140);
#1749=LINE('',#10003,#2141);
#1750=LINE('',#10004,#2142);
#2119=VECTOR('',#7028,0.325);
#2120=VECTOR('',#7033,0.35);
#2121=VECTOR('',#7038,0.335);
#2122=VECTOR('',#7047,0.21);
#2123=VECTOR('',#7052,0.2);
#2124=VECTOR('',#7057,0.18);
#2125=VECTOR('',#7062,1.);
#2126=VECTOR('',#7063,1.);
#2127=VECTOR('',#7064,1.);
#2128=VECTOR('',#7065,1.);
#2129=VECTOR('',#7068,1.);
#2130=VECTOR('',#7069,1.);
#2131=VECTOR('',#7070,1.);
#2132=VECTOR('',#7073,1.);
#2133=VECTOR('',#7074,1.);
#2134=VECTOR('',#7075,1.);
#2135=VECTOR('',#7078,1.);
#2136=VECTOR('',#7079,1.);
#2137=VECTOR('',#7080,1.);
#2138=VECTOR('',#7083,1.);
#2139=VECTOR('',#7084,1.);
#2140=VECTOR('',#7085,1.);
#2141=VECTOR('',#7088,1.);
#2142=VECTOR('',#7089,1.);
#2362=CIRCLE('',#5710,0.3);
#2363=CIRCLE('',#5712,0.35);
#2364=CIRCLE('',#5714,0.35);
#2365=CIRCLE('',#5716,0.32);
#2366=CIRCLE('',#5718,0.22);
#2367=CIRCLE('',#5720,0.1954);
#2368=CIRCLE('',#5722,0.1954);
#2369=CIRCLE('',#5724,0.16);
#2727=VERTEX_POINT('',#9939);
#2728=VERTEX_POINT('',#9942);
#2729=VERTEX_POINT('',#9946);
#2730=VERTEX_POINT('',#9950);
#2731=VERTEX_POINT('',#9954);
#2732=VERTEX_POINT('',#9957);
#2733=VERTEX_POINT('',#9961);
#2734=VERTEX_POINT('',#9965);
#2735=VERTEX_POINT('',#9970);
#2736=VERTEX_POINT('',#9971);
#2737=VERTEX_POINT('',#9973);
#2738=VERTEX_POINT('',#9975);
#2739=VERTEX_POINT('',#9979);
#2740=VERTEX_POINT('',#9981);
#2741=VERTEX_POINT('',#9985);
#2742=VERTEX_POINT('',#9987);
#2743=VERTEX_POINT('',#9991);
#2744=VERTEX_POINT('',#9993);
#2745=VERTEX_POINT('',#9997);
#2746=VERTEX_POINT('',#9999);
#3301=EDGE_CURVE('',#2727,#2727,#2362,.T.);
#3302=EDGE_CURVE('',#2728,#2728,#2363,.T.);
#3303=EDGE_CURVE('',#2728,#2727,#1727,.T.);
#3304=EDGE_CURVE('',#2729,#2729,#2364,.T.);
#3305=EDGE_CURVE('',#2729,#2728,#1728,.T.);
#3306=EDGE_CURVE('',#2730,#2730,#2365,.T.);
#3307=EDGE_CURVE('',#2730,#2729,#1729,.T.);
#3308=EDGE_CURVE('',#2731,#2731,#2366,.T.);
#3309=EDGE_CURVE('',#2732,#2732,#2367,.F.);
#3310=EDGE_CURVE('',#2732,#2731,#1730,.T.);
#3311=EDGE_CURVE('',#2733,#2733,#2368,.F.);
#3312=EDGE_CURVE('',#2733,#2732,#1731,.T.);
#3313=EDGE_CURVE('',#2734,#2734,#2369,.T.);
#3314=EDGE_CURVE('',#2734,#2733,#1732,.T.);
#3315=EDGE_CURVE('',#2735,#2736,#1733,.T.);
#3316=EDGE_CURVE('',#2736,#2737,#1734,.T.);
#3317=EDGE_CURVE('',#2737,#2738,#1735,.T.);
#3318=EDGE_CURVE('',#2735,#2738,#1736,.T.);
#3319=EDGE_CURVE('',#2736,#2739,#1737,.T.);
#3320=EDGE_CURVE('',#2739,#2740,#1738,.T.);
#3321=EDGE_CURVE('',#2740,#2737,#1739,.T.);
#3322=EDGE_CURVE('',#2739,#2741,#1740,.T.);
#3323=EDGE_CURVE('',#2741,#2742,#1741,.T.);
#3324=EDGE_CURVE('',#2742,#2740,#1742,.T.);
#3325=EDGE_CURVE('',#2741,#2743,#1743,.T.);
#3326=EDGE_CURVE('',#2743,#2744,#1744,.T.);
#3327=EDGE_CURVE('',#2744,#2742,#1745,.T.);
#3328=EDGE_CURVE('',#2743,#2745,#1746,.T.);
#3329=EDGE_CURVE('',#2745,#2746,#1747,.T.);
#3330=EDGE_CURVE('',#2746,#2744,#1748,.T.);
#3331=EDGE_CURVE('',#2745,#2735,#1749,.T.);
#3332=EDGE_CURVE('',#2738,#2746,#1750,.T.);
#4421=ORIENTED_EDGE('',*,*,#3301,.F.);
#4422=ORIENTED_EDGE('',*,*,#3302,.F.);
#4423=ORIENTED_EDGE('',*,*,#3303,.T.);
#4424=ORIENTED_EDGE('',*,*,#3301,.T.);
#4425=ORIENTED_EDGE('',*,*,#3303,.F.);
#4426=ORIENTED_EDGE('',*,*,#3304,.F.);
#4427=ORIENTED_EDGE('',*,*,#3305,.T.);
#4428=ORIENTED_EDGE('',*,*,#3302,.T.);
#4429=ORIENTED_EDGE('',*,*,#3305,.F.);
#4430=ORIENTED_EDGE('',*,*,#3306,.F.);
#4431=ORIENTED_EDGE('',*,*,#3307,.T.);
#4432=ORIENTED_EDGE('',*,*,#3304,.T.);
#4433=ORIENTED_EDGE('',*,*,#3307,.F.);
#4434=ORIENTED_EDGE('',*,*,#3306,.T.);
#4435=ORIENTED_EDGE('',*,*,#3308,.F.);
#4436=ORIENTED_EDGE('',*,*,#3309,.F.);
#4437=ORIENTED_EDGE('',*,*,#3310,.T.);
#4438=ORIENTED_EDGE('',*,*,#3308,.T.);
#4439=ORIENTED_EDGE('',*,*,#3310,.F.);
#4440=ORIENTED_EDGE('',*,*,#3311,.F.);
#4441=ORIENTED_EDGE('',*,*,#3312,.T.);
#4442=ORIENTED_EDGE('',*,*,#3309,.T.);
#4443=ORIENTED_EDGE('',*,*,#3312,.F.);
#4444=ORIENTED_EDGE('',*,*,#3313,.F.);
#4445=ORIENTED_EDGE('',*,*,#3314,.T.);
#4446=ORIENTED_EDGE('',*,*,#3311,.T.);
#4447=ORIENTED_EDGE('',*,*,#3314,.F.);
#4448=ORIENTED_EDGE('',*,*,#3313,.T.);
#4449=ORIENTED_EDGE('',*,*,#3315,.T.);
#4450=ORIENTED_EDGE('',*,*,#3316,.T.);
#4451=ORIENTED_EDGE('',*,*,#3317,.T.);
#4452=ORIENTED_EDGE('',*,*,#3318,.F.);
#4453=ORIENTED_EDGE('',*,*,#3319,.T.);
#4454=ORIENTED_EDGE('',*,*,#3320,.T.);
#4455=ORIENTED_EDGE('',*,*,#3321,.T.);
#4456=ORIENTED_EDGE('',*,*,#3316,.F.);
#4457=ORIENTED_EDGE('',*,*,#3322,.T.);
#4458=ORIENTED_EDGE('',*,*,#3323,.T.);
#4459=ORIENTED_EDGE('',*,*,#3324,.T.);
#4460=ORIENTED_EDGE('',*,*,#3320,.F.);
#4461=ORIENTED_EDGE('',*,*,#3325,.T.);
#4462=ORIENTED_EDGE('',*,*,#3326,.T.);
#4463=ORIENTED_EDGE('',*,*,#3327,.T.);
#4464=ORIENTED_EDGE('',*,*,#3323,.F.);
#4465=ORIENTED_EDGE('',*,*,#3328,.T.);
#4466=ORIENTED_EDGE('',*,*,#3329,.T.);
#4467=ORIENTED_EDGE('',*,*,#3330,.T.);
#4468=ORIENTED_EDGE('',*,*,#3326,.F.);
#4469=ORIENTED_EDGE('',*,*,#3331,.T.);
#4470=ORIENTED_EDGE('',*,*,#3318,.T.);
#4471=ORIENTED_EDGE('',*,*,#3332,.T.);
#4472=ORIENTED_EDGE('',*,*,#3329,.F.);
#4473=ORIENTED_EDGE('',*,*,#3331,.F.);
#4474=ORIENTED_EDGE('',*,*,#3328,.F.);
#4475=ORIENTED_EDGE('',*,*,#3325,.F.);
#4476=ORIENTED_EDGE('',*,*,#3322,.F.);
#4477=ORIENTED_EDGE('',*,*,#3319,.F.);
#4478=ORIENTED_EDGE('',*,*,#3315,.F.);
#4479=ORIENTED_EDGE('',*,*,#3332,.F.);
#4480=ORIENTED_EDGE('',*,*,#3317,.F.);
#4481=ORIENTED_EDGE('',*,*,#3321,.F.);
#4482=ORIENTED_EDGE('',*,*,#3324,.F.);
#4483=ORIENTED_EDGE('',*,*,#3327,.F.);
#4484=ORIENTED_EDGE('',*,*,#3330,.F.);
#4709=CYLINDRICAL_SURFACE('',#5713,0.35);
#4710=CYLINDRICAL_SURFACE('',#5721,0.1954);
#4948=ADVANCED_FACE('',(#939),#673,.T.);
#4949=ADVANCED_FACE('',(#940),#307,.T.);
#4950=ADVANCED_FACE('',(#941),#4709,.T.);
#4951=ADVANCED_FACE('',(#942),#308,.T.);
#4952=ADVANCED_FACE('',(#943,#524),#674,.T.);
#4953=ADVANCED_FACE('',(#944),#309,.T.);
#4954=ADVANCED_FACE('',(#945),#4710,.T.);
#4955=ADVANCED_FACE('',(#946),#310,.T.);
#4956=ADVANCED_FACE('',(#947),#675,.T.);
#4957=ADVANCED_FACE('',(#948),#676,.F.);
#4958=ADVANCED_FACE('',(#949),#677,.F.);
#4959=ADVANCED_FACE('',(#950),#678,.F.);
#4960=ADVANCED_FACE('',(#951),#679,.F.);
#4961=ADVANCED_FACE('',(#952),#680,.F.);
#4962=ADVANCED_FACE('',(#953),#681,.F.);
#4963=ADVANCED_FACE('',(#954),#682,.F.);
#4964=ADVANCED_FACE('',(#955),#683,.F.);
#5027=CLOSED_SHELL('',(#4948,#4949,#4950,#4951,#4952,#4953,#4954,#4955,
#4956));
#5028=CLOSED_SHELL('',(#4957,#4958,#4959,#4960,#4961,#4962,#4963,#4964));
#5708=AXIS2_PLACEMENT_3D('',#9937,#7018,#7019);
#5709=AXIS2_PLACEMENT_3D('',#9938,#7020,#7021);
#5710=AXIS2_PLACEMENT_3D('',#9940,#7022,#7023);
#5711=AXIS2_PLACEMENT_3D('',#9941,#7024,#7025);
#5712=AXIS2_PLACEMENT_3D('',#9943,#7026,#7027);
#5713=AXIS2_PLACEMENT_3D('',#9945,#7029,#7030);
#5714=AXIS2_PLACEMENT_3D('',#9947,#7031,#7032);
#5715=AXIS2_PLACEMENT_3D('',#9949,#7034,#7035);
#5716=AXIS2_PLACEMENT_3D('',#9951,#7036,#7037);
#5717=AXIS2_PLACEMENT_3D('',#9953,#7039,#7040);
#5718=AXIS2_PLACEMENT_3D('',#9955,#7041,#7042);
#5719=AXIS2_PLACEMENT_3D('',#9956,#7043,#7044);
#5720=AXIS2_PLACEMENT_3D('',#9958,#7045,#7046);
#5721=AXIS2_PLACEMENT_3D('',#9960,#7048,#7049);
#5722=AXIS2_PLACEMENT_3D('',#9962,#7050,#7051);
#5723=AXIS2_PLACEMENT_3D('',#9964,#7053,#7054);
#5724=AXIS2_PLACEMENT_3D('',#9966,#7055,#7056);
#5725=AXIS2_PLACEMENT_3D('',#9968,#7058,#7059);
#5726=AXIS2_PLACEMENT_3D('',#9969,#7060,#7061);
#5727=AXIS2_PLACEMENT_3D('',#9978,#7066,#7067);
#5728=AXIS2_PLACEMENT_3D('',#9984,#7071,#7072);
#5729=AXIS2_PLACEMENT_3D('',#9990,#7076,#7077);
#5730=AXIS2_PLACEMENT_3D('',#9996,#7081,#7082);
#5731=AXIS2_PLACEMENT_3D('',#10002,#7086,#7087);
#5732=AXIS2_PLACEMENT_3D('',#10005,#7090,#7091);
#5733=AXIS2_PLACEMENT_3D('',#10006,#7092,#7093);
#7018=DIRECTION('axis',(0.,0.,1.));
#7019=DIRECTION('refdir',(1.,0.,0.));
#7020=DIRECTION('center_axis',(0.,1.,0.));
#7021=DIRECTION('ref_axis',(0.,0.,1.));
#7022=DIRECTION('center_axis',(0.,-1.,0.));
#7023=DIRECTION('ref_axis',(1.,0.,0.));
#7024=DIRECTION('center_axis',(0.,-1.,0.));
#7025=DIRECTION('ref_axis',(1.,0.,0.));
#7026=DIRECTION('center_axis',(0.,-1.,0.));
#7027=DIRECTION('ref_axis',(1.,0.,0.));
#7028=DIRECTION('',(0.707106781186547,0.707106781186548,8.65956056235493E-17));
#7029=DIRECTION('center_axis',(0.,-1.,0.));
#7030=DIRECTION('ref_axis',(1.,0.,0.));
#7031=DIRECTION('center_axis',(0.,-1.,0.));
#7032=DIRECTION('ref_axis',(1.,0.,0.));
#7033=DIRECTION('',(0.,1.,0.));
#7034=DIRECTION('center_axis',(0.,1.,0.));
#7035=DIRECTION('ref_axis',(1.,0.,0.));
#7036=DIRECTION('center_axis',(0.,-1.,0.));
#7037=DIRECTION('ref_axis',(1.,0.,0.));
#7038=DIRECTION('',(-0.707106781186547,0.707106781186548,-8.65956056235493E-17));
#7039=DIRECTION('center_axis',(0.,-1.,0.));
#7040=DIRECTION('ref_axis',(0.,0.,-1.));
#7041=DIRECTION('center_axis',(0.,-1.,0.));
#7042=DIRECTION('ref_axis',(1.,0.,0.));
#7043=DIRECTION('center_axis',(0.,1.,0.));
#7044=DIRECTION('ref_axis',(1.,0.,0.));
#7045=DIRECTION('center_axis',(0.,1.,0.));
#7046=DIRECTION('ref_axis',(1.,0.,0.));
#7047=DIRECTION('',(-0.447213595499958,0.894427190999916,-5.47678698264203E-17));
#7048=DIRECTION('center_axis',(0.,-1.,0.));
#7049=DIRECTION('ref_axis',(1.,0.,0.));
#7050=DIRECTION('center_axis',(0.,1.,0.));
#7051=DIRECTION('ref_axis',(1.,0.,0.));
#7052=DIRECTION('',(0.,1.,0.));
#7053=DIRECTION('center_axis',(0.,1.,0.));
#7054=DIRECTION('ref_axis',(1.,0.,0.));
#7055=DIRECTION('center_axis',(0.,-1.,0.));
#7056=DIRECTION('ref_axis',(1.,0.,0.));
#7057=DIRECTION('',(-0.707106781186547,0.707106781186548,-8.65956056235493E-17));
#7058=DIRECTION('center_axis',(0.,-1.,0.));
#7059=DIRECTION('ref_axis',(0.,0.,-1.));
#7060=DIRECTION('center_axis',(0.866025403784439,0.,-0.5));
#7061=DIRECTION('ref_axis',(0.5,0.,0.866025403784439));
#7062=DIRECTION('',(-0.5,0.,-0.866025403784439));
#7063=DIRECTION('',(0.,-1.,0.));
#7064=DIRECTION('',(0.5,0.,0.866025403784439));
#7065=DIRECTION('',(0.,-1.,0.));
#7066=DIRECTION('center_axis',(1.60246890531964E-16,0.,-1.));
#7067=DIRECTION('ref_axis',(1.,0.,1.60246890531964E-16));
#7068=DIRECTION('',(-1.,0.,-1.60246890531964E-16));
#7069=DIRECTION('',(0.,-1.,0.));
#7070=DIRECTION('',(1.,0.,1.60246890531964E-16));
#7071=DIRECTION('center_axis',(-0.866025403784439,0.,-0.5));
#7072=DIRECTION('ref_axis',(0.5,0.,-0.866025403784439));
#7073=DIRECTION('',(-0.5,0.,0.866025403784439));
#7074=DIRECTION('',(0.,-1.,0.));
#7075=DIRECTION('',(0.5,0.,-0.866025403784439));
#7076=DIRECTION('center_axis',(-0.866025403784439,0.,0.5));
#7077=DIRECTION('ref_axis',(-0.5,0.,-0.866025403784439));
#7078=DIRECTION('',(0.5,0.,0.866025403784439));
#7079=DIRECTION('',(0.,-1.,0.));
#7080=DIRECTION('',(-0.5,0.,-0.866025403784439));
#7081=DIRECTION('center_axis',(-1.60246890531964E-16,0.,1.));
#7082=DIRECTION('ref_axis',(-1.,0.,-1.60246890531964E-16));
#7083=DIRECTION('',(1.,0.,1.60246890531964E-16));
#7084=DIRECTION('',(0.,-1.,0.));
#7085=DIRECTION('',(-1.,0.,-1.60246890531964E-16));
#7086=DIRECTION('center_axis',(0.866025403784439,0.,0.5));
#7087=DIRECTION('ref_axis',(-0.5,0.,0.866025403784439));
#7088=DIRECTION('',(0.5,0.,-0.866025403784439));
#7089=DIRECTION('',(-0.5,0.,0.866025403784439));
#7090=DIRECTION('center_axis',(0.,1.,0.));
#7091=DIRECTION('ref_axis',(1.,0.,0.));
#7092=DIRECTION('center_axis',(0.,-1.,0.));
#7093=DIRECTION('ref_axis',(0.,0.,-1.));
#9937=CARTESIAN_POINT('',(0.,0.,0.));
#9938=CARTESIAN_POINT('Origin',(0.3,0.4,0.));
#9939=CARTESIAN_POINT('',(-0.3,0.4,-3.67394039744206E-17));
#9940=CARTESIAN_POINT('Origin',(0.,0.4,0.));
#9941=CARTESIAN_POINT('Origin',(0.,0.375,0.));
#9942=CARTESIAN_POINT('',(-0.35,0.35,-4.28626379701573E-17));
#9943=CARTESIAN_POINT('Origin',(0.,0.35,0.));
#9944=CARTESIAN_POINT('',(-0.325,0.375,-3.9801020972289E-17));
#9945=CARTESIAN_POINT('Origin',(0.,0.19,0.));
#9946=CARTESIAN_POINT('',(-0.35,0.03,-4.28626379701574E-17));
#9947=CARTESIAN_POINT('Origin',(0.,0.03,0.));
#9948=CARTESIAN_POINT('',(-0.35,0.19,-4.28626379701574E-17));
#9949=CARTESIAN_POINT('Origin',(0.,0.0149999999999999,0.));
#9950=CARTESIAN_POINT('',(-0.32,-3.29597460435593E-17,-3.91886975727153E-17));
#9951=CARTESIAN_POINT('Origin',(0.,0.,0.));
#9952=CARTESIAN_POINT('',(-0.335,0.0149999999999999,-4.10256677714363E-17));
#9953=CARTESIAN_POINT('Origin',(0.22,0.,0.));
#9954=CARTESIAN_POINT('',(-0.22,-6.93889390390723E-18,-2.69422295812418E-17));
#9955=CARTESIAN_POINT('Origin',(0.,0.,0.));
#9956=CARTESIAN_POINT('Origin',(0.,-0.02,0.));
#9957=CARTESIAN_POINT('',(-0.1954,-0.0492,2.39295984553393E-17));
#9958=CARTESIAN_POINT('Origin',(0.,-0.0492,0.));
#9959=CARTESIAN_POINT('',(-0.21,-0.02,-2.57175827820944E-17));
#9960=CARTESIAN_POINT('Origin',(0.,-0.8,0.));
#9961=CARTESIAN_POINT('',(-0.1954,-1.5646,2.39295984553393E-17));
#9962=CARTESIAN_POINT('Origin',(0.,-1.5646,0.));
#9963=CARTESIAN_POINT('',(-0.1954,-0.8,-2.39295984553393E-17));
#9964=CARTESIAN_POINT('Origin',(0.,-1.58,0.));
#9965=CARTESIAN_POINT('',(-0.16,-1.6,-1.95943487863577E-17));
#9966=CARTESIAN_POINT('Origin',(0.,-1.6,0.));
#9967=CARTESIAN_POINT('',(-0.18,-1.58,-2.20436423846524E-17));
#9968=CARTESIAN_POINT('Origin',(0.,-1.6,0.));
#9969=CARTESIAN_POINT('Origin',(0.0866025403784439,-0.4,-0.15));
#9970=CARTESIAN_POINT('',(0.173205080756888,-0.4,0.));
#9971=CARTESIAN_POINT('',(0.0866025403784439,-0.4,-0.15));
#9972=CARTESIAN_POINT('',(0.173205080756888,-0.4,0.));
#9973=CARTESIAN_POINT('',(0.0866025403784439,-0.64,-0.15));
#9974=CARTESIAN_POINT('',(0.0866025403784439,-0.4,-0.15));
#9975=CARTESIAN_POINT('',(0.173205080756888,-0.64,0.));
#9976=CARTESIAN_POINT('',(0.173205080756888,-0.64,0.));
#9977=CARTESIAN_POINT('',(0.173205080756888,-0.4,0.));
#9978=CARTESIAN_POINT('Origin',(-0.0866025403784438,-0.4,-0.15));
#9979=CARTESIAN_POINT('',(-0.0866025403784438,-0.4,-0.15));
#9980=CARTESIAN_POINT('',(0.0866025403784439,-0.4,-0.15));
#9981=CARTESIAN_POINT('',(-0.0866025403784438,-0.64,-0.15));
#9982=CARTESIAN_POINT('',(-0.0866025403784438,-0.4,-0.15));
#9983=CARTESIAN_POINT('',(0.0866025403784439,-0.64,-0.15));
#9984=CARTESIAN_POINT('Origin',(-0.173205080756888,-0.4,-2.77555756156289E-17));
#9985=CARTESIAN_POINT('',(-0.173205080756888,-0.4,-2.12115047744981E-17));
#9986=CARTESIAN_POINT('',(-0.0866025403784438,-0.4,-0.15));
#9987=CARTESIAN_POINT('',(-0.173205080756888,-0.64,-2.77555756156289E-17));
#9988=CARTESIAN_POINT('',(-0.173205080756888,-0.4,-2.12115047744981E-17));
#9989=CARTESIAN_POINT('',(-0.0866025403784438,-0.64,-0.15));
#9990=CARTESIAN_POINT('Origin',(-0.0866025403784439,-0.4,0.15));
#9991=CARTESIAN_POINT('',(-0.0866025403784439,-0.4,0.15));
#9992=CARTESIAN_POINT('',(-0.173205080756888,-0.4,-2.12115047744981E-17));
#9993=CARTESIAN_POINT('',(-0.0866025403784439,-0.64,0.15));
#9994=CARTESIAN_POINT('',(-0.0866025403784439,-0.4,0.15));
#9995=CARTESIAN_POINT('',(-0.173205080756888,-0.64,-2.12115047744981E-17));
#9996=CARTESIAN_POINT('Origin',(0.0866025403784439,-0.4,0.15));
#9997=CARTESIAN_POINT('',(0.0866025403784439,-0.4,0.15));
#9998=CARTESIAN_POINT('',(-0.0866025403784439,-0.4,0.15));
#9999=CARTESIAN_POINT('',(0.0866025403784439,-0.64,0.15));
#10000=CARTESIAN_POINT('',(0.0866025403784439,-0.4,0.15));
#10001=CARTESIAN_POINT('',(-0.0866025403784439,-0.64,0.15));
#10002=CARTESIAN_POINT('Origin',(0.173205080756888,-0.4,0.));
#10003=CARTESIAN_POINT('',(0.0866025403784439,-0.4,0.15));
#10004=CARTESIAN_POINT('',(0.0866025403784439,-0.64,0.15));
#10005=CARTESIAN_POINT('Origin',(0.,-0.4,-2.77555756156289E-17));
#10006=CARTESIAN_POINT('Origin',(0.,-0.64,-2.77555756156289E-17));
#10259=UNCERTAINTY_MEASURE_WITH_UNIT(LENGTH_MEASURE(0.001),#10293,
'DISTANCE_ACCURACY_VALUE',
'Maximum model space distance between geometric entities at asserted c
onnectivities');
#10264=UNCERTAINTY_MEASURE_WITH_UNIT(LENGTH_MEASURE(0.001),#10293,
'DISTANCE_ACCURACY_VALUE',
'Maximum model space distance between geometric entities at asserted c
onnectivities');
#10287=(
GEOMETRIC_REPRESENTATION_CONTEXT(3)
GLOBAL_UNCERTAINTY_ASSIGNED_CONTEXT((#10259))
GLOBAL_UNIT_ASSIGNED_CONTEXT((#10293,#10295,#10296))
REPRESENTATION_CONTEXT('','3D')
);
#10292=(
GEOMETRIC_REPRESENTATION_CONTEXT(3)
GLOBAL_UNCERTAINTY_ASSIGNED_CONTEXT((#10264))
GLOBAL_UNIT_ASSIGNED_CONTEXT((#10293,#10295,#10296))
REPRESENTATION_CONTEXT('','3D')
);
#10293=(
LENGTH_UNIT()
NAMED_UNIT(*)
SI_UNIT(.CENTI.,.METRE.)
);
#10295=(
NAMED_UNIT(*)
PLANE_ANGLE_UNIT()
SI_UNIT($,.RADIAN.)
);
#10296=(
NAMED_UNIT(*)
SI_UNIT($,.STERADIAN.)
SOLID_ANGLE_UNIT()
);
#10319=SHAPE_DEFINITION_REPRESENTATION(#10348,#10435);
#10348=PRODUCT_DEFINITION_SHAPE('',$,#10463);
#10435=SHAPE_REPRESENTATION('',(#5708),#10287);
#10440=PRODUCT_DEFINITION_CONTEXT('part definition',#10523,'design');
#10463=PRODUCT_DEFINITION('Cap Screw - M4x16','Cap Screw - M4x16',
#10490,#10440);
#10490=PRODUCT_DEFINITION_FORMATION('',$,#10547);
#10523=APPLICATION_CONTEXT(
'Core Data for Automotive Mechanical Design Process');
#10524=PRODUCT_CONTEXT('part definition',#10523,'mechanical');
#10547=PRODUCT('Cap Screw - M4x16','Cap Screw - M4x16',
'Cap Screw - M4x16',(#10524));
#10629=COLOUR_RGB('Black',0.12,0.14,0.17);
#10630=FILL_AREA_STYLE_COLOUR('',#10629);
#10631=FILL_AREA_STYLE('',(#10630));
#10632=SURFACE_STYLE_FILL_AREA(#10631);
#10633=SURFACE_SIDE_STYLE('',(#10632));
#10634=SURFACE_STYLE_USAGE(.BOTH.,#10633);
#10635=PRESENTATION_STYLE_ASSIGNMENT((#10634));
ENDSEC;
END-ISO-10303-21;
